ISO-10303-21;
HEADER;
/* Generated by software containing ST-Developer
 * from STEP Tools, Inc. (www.steptools.com) 
 */

FILE_DESCRIPTION(
/* description */ (''),
/* implementation_level */ '2;1');

FILE_NAME(
/* name */ 'Nut_01.step',
/* time_stamp */ '2026-10-05T16:20:14-07:00',
/* author */ (''),
/* organization */ (''),
/* preprocessor_version */ 'ST-DEVELOPER v20.2',
/* originating_system */ 'Autodesk Translation Framework v15.15.0.0',
/* authorisation */ '');

FILE_SCHEMA (('AUTOMOTIVE_DESIGN { 1 0 10303 214 3 1 1 }'));
ENDSEC;

DATA;
#10=MECHANICAL_DESIGN_GEOMETRIC_PRESENTATION_REPRESENTATION('',(#250),#23577);
#232=SHAPE_REPRESENTATION_RELATIONSHIP('SRR','None',#23615,#241);
#241=ADVANCED_BREP_SHAPE_REPRESENTATION('',(#259),#23571);
#250=STYLED_ITEM('',(#23666),#259);
#259=MANIFOLD_SOLID_BREP('Body1',#4160);
#281=FACE_BOUND('',#724,.T.);
#282=FACE_BOUND('',#726,.T.);
#342=PLANE('',#4428);
#343=PLANE('',#4429);
#344=PLANE('',#4430);
#345=PLANE('',#4431);
#346=PLANE('',#4432);
#347=PLANE('',#4433);
#348=PLANE('',#4434);
#349=PLANE('',#4435);
#474=FACE_OUTER_BOUND('',#716,.T.);
#475=FACE_OUTER_BOUND('',#717,.T.);
#476=FACE_OUTER_BOUND('',#718,.T.);
#477=FACE_OUTER_BOUND('',#719,.T.);
#478=FACE_OUTER_BOUND('',#720,.T.);
#479=FACE_OUTER_BOUND('',#721,.T.);
#480=FACE_OUTER_BOUND('',#722,.T.);
#481=FACE_OUTER_BOUND('',#723,.T.);
#482=FACE_OUTER_BOUND('',#725,.T.);
#716=EDGE_LOOP('',(#3037,#3038,#3039,#3040));
#717=EDGE_LOOP('',(#3041,#3042,#3043,#3044));
#718=EDGE_LOOP('',(#3045,#3046,#3047,#3048));
#719=EDGE_LOOP('',(#3049,#3050,#3051,#3052));
#720=EDGE_LOOP('',(#3053,#3054,#3055,#3056));
#721=EDGE_LOOP('',(#3057,#3058,#3059,#3060));
#722=EDGE_LOOP('',(#3061,#3062,#3063,#3064));
#723=EDGE_LOOP('',(#3065,#3066,#3067,#3068,#3069,#3070));
#724=EDGE_LOOP('',(#3071));
#725=EDGE_LOOP('',(#3072,#3073,#3074,#3075,#3076,#3077));
#726=EDGE_LOOP('',(#3078));
#1007=LINE('',#6194,#1292);
#1008=LINE('',#6199,#1293);
#1009=LINE('',#6201,#1294);
#1010=LINE('',#6203,#1295);
#1011=LINE('',#6204,#1296);
#1012=LINE('',#6207,#1297);
#1013=LINE('',#6209,#1298);
#1014=LINE('',#6210,#1299);
#1015=LINE('',#6213,#1300);
#1016=LINE('',#6215,#1301);
#1017=LINE('',#6216,#1302);
#1018=LINE('',#6219,#1303);
#1019=LINE('',#6221,#1304);
#1020=LINE('',#6222,#1305);
#1021=LINE('',#6225,#1306);
#1022=LINE('',#6227,#1307);
#1023=LINE('',#6228,#1308);
#1024=LINE('',#6230,#1309);
#1025=LINE('',#6231,#1310);
#1292=VECTOR('',#5120,2.5);
#1293=VECTOR('',#5125,9.99999999999999);
#1294=VECTOR('',#5126,10.);
#1295=VECTOR('',#5127,9.99999999999999);
#1296=VECTOR('',#5128,10.);
#1297=VECTOR('',#5131,10.);
#1298=VECTOR('',#5132,10.);
#1299=VECTOR('',#5133,10.);
#1300=VECTOR('',#5136,10.);
#1301=VECTOR('',#5137,10.);
#1302=VECTOR('',#5138,10.);
#1303=VECTOR('',#5141,10.);
#1304=VECTOR('',#5142,10.);
#1305=VECTOR('',#5143,10.);
#1306=VECTOR('',#5146,10.);
#1307=VECTOR('',#5147,10.);
#1308=VECTOR('',#5148,10.);
#1309=VECTOR('',#5151,10.);
#1310=VECTOR('',#5152,10.);
#1525=CIRCLE('',#4426,2.5);
#1526=CIRCLE('',#4427,2.5);
#1760=VERTEX_POINT('',#6191);
#1761=VERTEX_POINT('',#6193);
#1762=VERTEX_POINT('',#6197);
#1763=VERTEX_POINT('',#6198);
#1764=VERTEX_POINT('',#6200);
#1765=VERTEX_POINT('',#6202);
#1766=VERTEX_POINT('',#6206);
#1767=VERTEX_POINT('',#6208);
#1768=VERTEX_POINT('',#6212);
#1769=VERTEX_POINT('',#6214);
#1770=VERTEX_POINT('',#6218);
#1771=VERTEX_POINT('',#6220);
#1772=VERTEX_POINT('',#6224);
#1773=VERTEX_POINT('',#6226);
#2235=EDGE_CURVE('',#1760,#1760,#1525,.T.);
#2236=EDGE_CURVE('',#1760,#1761,#1007,.T.);
#2237=EDGE_CURVE('',#1761,#1761,#1526,.T.);
#2238=EDGE_CURVE('',#1762,#1763,#1008,.T.);
#2239=EDGE_CURVE('',#1762,#1764,#1009,.T.);
#2240=EDGE_CURVE('',#1765,#1764,#1010,.T.);
#2241=EDGE_CURVE('',#1763,#1765,#1011,.T.);
#2242=EDGE_CURVE('',#1763,#1766,#1012,.T.);
#2243=EDGE_CURVE('',#1767,#1765,#1013,.T.);
#2244=EDGE_CURVE('',#1766,#1767,#1014,.T.);
#2245=EDGE_CURVE('',#1766,#1768,#1015,.T.);
#2246=EDGE_CURVE('',#1769,#1767,#1016,.T.);
#2247=EDGE_CURVE('',#1768,#1769,#1017,.T.);
#2248=EDGE_CURVE('',#1768,#1770,#1018,.T.);
#2249=EDGE_CURVE('',#1771,#1769,#1019,.T.);
#2250=EDGE_CURVE('',#1770,#1771,#1020,.T.);
#2251=EDGE_CURVE('',#1770,#1772,#1021,.T.);
#2252=EDGE_CURVE('',#1773,#1771,#1022,.T.);
#2253=EDGE_CURVE('',#1772,#1773,#1023,.T.);
#2254=EDGE_CURVE('',#1772,#1762,#1024,.T.);
#2255=EDGE_CURVE('',#1764,#1773,#1025,.T.);
#3037=ORIENTED_EDGE('',*,*,#2235,.F.);
#3038=ORIENTED_EDGE('',*,*,#2236,.T.);
#3039=ORIENTED_EDGE('',*,*,#2237,.F.);
#3040=ORIENTED_EDGE('',*,*,#2236,.F.);
#3041=ORIENTED_EDGE('',*,*,#2238,.F.);
#3042=ORIENTED_EDGE('',*,*,#2239,.T.);
#3043=ORIENTED_EDGE('',*,*,#2240,.F.);
#3044=ORIENTED_EDGE('',*,*,#2241,.F.);
#3045=ORIENTED_EDGE('',*,*,#2242,.F.);
#3046=ORIENTED_EDGE('',*,*,#2241,.T.);
#3047=ORIENTED_EDGE('',*,*,#2243,.F.);
#3048=ORIENTED_EDGE('',*,*,#2244,.F.);
#3049=ORIENTED_EDGE('',*,*,#2245,.F.);
#3050=ORIENTED_EDGE('',*,*,#2244,.T.);
#3051=ORIENTED_EDGE('',*,*,#2246,.F.);
#3052=ORIENTED_EDGE('',*,*,#2247,.F.);
#3053=ORIENTED_EDGE('',*,*,#2248,.F.);
#3054=ORIENTED_EDGE('',*,*,#2247,.T.);
#3055=ORIENTED_EDGE('',*,*,#2249,.F.);
#3056=ORIENTED_EDGE('',*,*,#2250,.F.);
#3057=ORIENTED_EDGE('',*,*,#2251,.F.);
#3058=ORIENTED_EDGE('',*,*,#2250,.T.);
#3059=ORIENTED_EDGE('',*,*,#2252,.F.);
#3060=ORIENTED_EDGE('',*,*,#2253,.F.);
#3061=ORIENTED_EDGE('',*,*,#2254,.F.);
#3062=ORIENTED_EDGE('',*,*,#2253,.T.);
#3063=ORIENTED_EDGE('',*,*,#2255,.F.);
#3064=ORIENTED_EDGE('',*,*,#2239,.F.);
#3065=ORIENTED_EDGE('',*,*,#2254,.T.);
#3066=ORIENTED_EDGE('',*,*,#2238,.T.);
#3067=ORIENTED_EDGE('',*,*,#2242,.T.);
#3068=ORIENTED_EDGE('',*,*,#2245,.T.);
#3069=ORIENTED_EDGE('',*,*,#2248,.T.);
#3070=ORIENTED_EDGE('',*,*,#2251,.T.);
#3071=ORIENTED_EDGE('',*,*,#2235,.T.);
#3072=ORIENTED_EDGE('',*,*,#2255,.T.);
#3073=ORIENTED_EDGE('',*,*,#2252,.T.);
#3074=ORIENTED_EDGE('',*,*,#2249,.T.);
#3075=ORIENTED_EDGE('',*,*,#2246,.T.);
#3076=ORIENTED_EDGE('',*,*,#2243,.T.);
#3077=ORIENTED_EDGE('',*,*,#2240,.T.);
#3078=ORIENTED_EDGE('',*,*,#2237,.T.);
#3873=CYLINDRICAL_SURFACE('',#4425,2.5);
#4009=ADVANCED_FACE('',(#474),#3873,.F.);
#4010=ADVANCED_FACE('',(#475),#342,.T.);
#4011=ADVANCED_FACE('',(#476),#343,.T.);
#4012=ADVANCED_FACE('',(#477),#344,.T.);
#4013=ADVANCED_FACE('',(#478),#345,.T.);
#4014=ADVANCED_FACE('',(#479),#346,.T.);
#4015=ADVANCED_FACE('',(#480),#347,.T.);
#4016=ADVANCED_FACE('',(#481,#281),#348,.T.);
#4017=ADVANCED_FACE('',(#482,#282),#349,.F.);
#4160=CLOSED_SHELL('',(#4009,#4010,#4011,#4012,#4013,#4014,#4015,#4016,
#4017));
#4424=AXIS2_PLACEMENT_3D('',#6189,#5114,#5115);
#4425=AXIS2_PLACEMENT_3D('',#6190,#5116,#5117);
#4426=AXIS2_PLACEMENT_3D('',#6192,#5118,#5119);
#4427=AXIS2_PLACEMENT_3D('',#6195,#5121,#5122);
#4428=AXIS2_PLACEMENT_3D('',#6196,#5123,#5124);
#4429=AXIS2_PLACEMENT_3D('',#6205,#5129,#5130);
#4430=AXIS2_PLACEMENT_3D('',#6211,#5134,#5135);
#4431=AXIS2_PLACEMENT_3D('',#6217,#5139,#5140);
#4432=AXIS2_PLACEMENT_3D('',#6223,#5144,#5145);
#4433=AXIS2_PLACEMENT_3D('',#6229,#5149,#5150);
#4434=AXIS2_PLACEMENT_3D('',#6232,#5153,#5154);
#4435=AXIS2_PLACEMENT_3D('',#6233,#5155,#5156);
#5114=DIRECTION('axis',(0.,0.,1.));
#5115=DIRECTION('refdir',(1.,0.,0.));
#5116=DIRECTION('center_axis',(0.,0.,-1.));
#5117=DIRECTION('ref_axis',(-1.,0.,0.));
#5118=DIRECTION('center_axis',(0.,0.,-1.));
#5119=DIRECTION('ref_axis',(-1.,0.,0.));
#5120=DIRECTION('',(0.,0.,-1.));
#5121=DIRECTION('center_axis',(0.,0.,1.));
#5122=DIRECTION('ref_axis',(-1.,0.,0.));
#5123=DIRECTION('center_axis',(0.866025403784439,-0.5,0.));
#5124=DIRECTION('ref_axis',(-0.5,-0.866025403784439,0.));
#5125=DIRECTION('',(0.5,0.866025403784439,0.));
#5126=DIRECTION('',(0.,0.,-1.));
#5127=DIRECTION('',(-0.5,-0.866025403784439,0.));
#5128=DIRECTION('',(0.,0.,-1.));
#5129=DIRECTION('center_axis',(0.866025403784439,0.5,0.));
#5130=DIRECTION('ref_axis',(0.5,-0.866025403784439,0.));
#5131=DIRECTION('',(-0.5,0.866025403784439,0.));
#5132=DIRECTION('',(0.5,-0.866025403784439,0.));
#5133=DIRECTION('',(0.,0.,-1.));
#5134=DIRECTION('center_axis',(4.80740671595891E-16,1.,0.));
#5135=DIRECTION('ref_axis',(1.,-4.80740671595891E-16,0.));
#5136=DIRECTION('',(-1.,4.80740671595891E-16,0.));
#5137=DIRECTION('',(1.,-4.80740671595891E-16,0.));
#5138=DIRECTION('',(0.,0.,-1.));
#5139=DIRECTION('center_axis',(-0.866025403784438,0.500000000000001,0.));
#5140=DIRECTION('ref_axis',(0.500000000000001,0.866025403784438,0.));
#5141=DIRECTION('',(-0.500000000000001,-0.866025403784438,0.));
#5142=DIRECTION('',(0.500000000000001,0.866025403784438,0.));
#5143=DIRECTION('',(0.,0.,-1.));
#5144=DIRECTION('center_axis',(-0.866025403784439,-0.499999999999999,0.));
#5145=DIRECTION('ref_axis',(-0.499999999999999,0.866025403784439,0.));
#5146=DIRECTION('',(0.499999999999999,-0.866025403784439,0.));
#5147=DIRECTION('',(-0.499999999999999,0.866025403784439,0.));
#5148=DIRECTION('',(0.,0.,-1.));
#5149=DIRECTION('center_axis',(-1.20185167898973E-16,-1.,0.));
#5150=DIRECTION('ref_axis',(-1.,1.20185167898973E-16,0.));
#5151=DIRECTION('',(1.,-1.20185167898973E-16,0.));
#5152=DIRECTION('',(-1.,1.20185167898973E-16,0.));
#5153=DIRECTION('center_axis',(0.,0.,1.));
#5154=DIRECTION('ref_axis',(-1.,0.,0.));
#5155=DIRECTION('center_axis',(0.,0.,1.));
#5156=DIRECTION('ref_axis',(-1.,0.,0.));
#6189=CARTESIAN_POINT('',(0.,0.,0.));
#6190=CARTESIAN_POINT('Origin',(5.09382715545311,0.,8.60636253116605));
#6191=CARTESIAN_POINT('',(7.59382715545311,3.06161699786838E-16,8.60636253116605));
#6192=CARTESIAN_POINT('Origin',(5.09382715545311,0.,8.60636253116605));
#6193=CARTESIAN_POINT('',(7.59382715545311,3.06161699786838E-16,5.60636253116605));
#6194=CARTESIAN_POINT('',(7.59382715545311,-3.06161699786838E-16,8.60636253116605));
#6195=CARTESIAN_POINT('Origin',(5.09382715545311,0.,5.60636253116605));
#6196=CARTESIAN_POINT('Origin',(9.71262930897012,-1.11022302462516E-15,
8.60636253116605));
#6197=CARTESIAN_POINT('',(7.40322823221161,-4.,8.60636253116605));
#6198=CARTESIAN_POINT('',(9.71262930897012,-1.11022302462516E-15,8.60636253116605));
#6199=CARTESIAN_POINT('',(7.40322823221161,-4.,8.60636253116605));
#6200=CARTESIAN_POINT('',(7.40322823221161,-4.,5.60636253116605));
#6201=CARTESIAN_POINT('',(7.40322823221161,-4.,8.60636253116605));
#6202=CARTESIAN_POINT('',(9.71262930897012,-1.11022302462516E-15,5.60636253116605));
#6203=CARTESIAN_POINT('',(7.40322823221161,-4.,5.60636253116605));
#6204=CARTESIAN_POINT('',(9.71262930897012,-1.11022302462516E-15,8.60636253116605));
#6205=CARTESIAN_POINT('Origin',(7.40322823221161,4.,8.60636253116605));
#6206=CARTESIAN_POINT('',(7.40322823221161,4.,8.60636253116605));
#6207=CARTESIAN_POINT('',(9.71262930897012,-1.11022302462516E-15,8.60636253116605));
#6208=CARTESIAN_POINT('',(7.40322823221161,4.,5.60636253116605));
#6209=CARTESIAN_POINT('',(9.71262930897012,-1.11022302462516E-15,5.60636253116605));
#6210=CARTESIAN_POINT('',(7.40322823221161,4.,8.60636253116605));
#6211=CARTESIAN_POINT('Origin',(2.78442607869461,4.,8.60636253116605));
#6212=CARTESIAN_POINT('',(2.78442607869461,4.,8.60636253116605));
#6213=CARTESIAN_POINT('',(7.40322823221161,4.,8.60636253116605));
#6214=CARTESIAN_POINT('',(2.78442607869461,4.,5.60636253116605));
#6215=CARTESIAN_POINT('',(7.40322823221161,4.,5.60636253116605));
#6216=CARTESIAN_POINT('',(2.78442607869461,4.,8.60636253116605));
#6217=CARTESIAN_POINT('Origin',(0.4750250019361,2.77555756156289E-15,8.60636253116605));
#6218=CARTESIAN_POINT('',(0.4750250019361,2.77555756156289E-15,8.60636253116605));
#6219=CARTESIAN_POINT('',(2.78442607869461,4.,8.60636253116605));
#6220=CARTESIAN_POINT('',(0.4750250019361,2.77555756156289E-15,5.60636253116605));
#6221=CARTESIAN_POINT('',(2.78442607869461,4.,5.60636253116605));
#6222=CARTESIAN_POINT('',(0.4750250019361,2.77555756156289E-15,8.60636253116605));
#6223=CARTESIAN_POINT('Origin',(2.7844260786946,-4.,8.60636253116605));
#6224=CARTESIAN_POINT('',(2.7844260786946,-4.,8.60636253116605));
#6225=CARTESIAN_POINT('',(0.4750250019361,2.77555756156289E-15,8.60636253116605));
#6226=CARTESIAN_POINT('',(2.7844260786946,-4.,5.60636253116605));
#6227=CARTESIAN_POINT('',(0.4750250019361,2.77555756156289E-15,5.60636253116605));
#6228=CARTESIAN_POINT('',(2.7844260786946,-4.,8.60636253116605));
#6229=CARTESIAN_POINT('Origin',(7.40322823221161,-4.,8.60636253116605));
#6230=CARTESIAN_POINT('',(2.7844260786946,-4.,8.60636253116605));
#6231=CARTESIAN_POINT('',(2.7844260786946,-4.,5.60636253116605));
#6232=CARTESIAN_POINT('Origin',(5.09382715545311,5.55111512312578E-16,8.60636253116605));
#6233=CARTESIAN_POINT('Origin',(5.09382715545311,5.55111512312578E-16,5.60636253116605));
#23560=UNCERTAINTY_MEASURE_WITH_UNIT(LENGTH_MEASURE(0.01),#23578,
'DISTANCE_ACCURACY_VALUE',
'Maximum model space distance between geometric entities at asserted c
onnectivities');
#23566=UNCERTAINTY_MEASURE_WITH_UNIT(LENGTH_MEASURE(0.01),#23578,
'DISTANCE_ACCURACY_VALUE',
'Maximum model space distance between geometric entities at asserted c
onnectivities');
#23571=(
GEOMETRIC_REPRESENTATION_CONTEXT(3)
GLOBAL_UNCERTAINTY_ASSIGNED_CONTEXT((#23560))
GLOBAL_UNIT_ASSIGNED_CONTEXT((#23578,#23580,#23581))
REPRESENTATION_CONTEXT('','3D')
);
#23577=(
GEOMETRIC_REPRESENTATION_CONTEXT(3)
GLOBAL_UNCERTAINTY_ASSIGNED_CONTEXT((#23566))
GLOBAL_UNIT_ASSIGNED_CONTEXT((#23578,#23580,#23581))
REPRESENTATION_CONTEXT('','3D')
);
#23578=(
LENGTH_UNIT()
NAMED_UNIT(*)
SI_UNIT(.MILLI.,.METRE.)
);
#23580=(
NAMED_UNIT(*)
PLANE_ANGLE_UNIT()
SI_UNIT($,.RADIAN.)
);
#23581=(
NAMED_UNIT(*)
SI_UNIT($,.STERADIAN.)
SOLID_ANGLE_UNIT()
);
#23586=SHAPE_DEFINITION_REPRESENTATION(#23596,#23615);
#23596=PRODUCT_DEFINITION_SHAPE('',$,#23626);
#23615=SHAPE_REPRESENTATION('',(#4424),#23571);
#23621=PRODUCT_DEFINITION_CONTEXT('part definition',#23653,'design');
#23626=PRODUCT_DEFINITION('Nut_01','Nut_01',#23636,#23621);
#23636=PRODUCT_DEFINITION_FORMATION('',$,#23659);
#23653=APPLICATION_CONTEXT(
'Core Data for Automotive Mechanical Design Process');
#23654=PRODUCT_CONTEXT('part definition',#23653,'mechanical');
#23659=PRODUCT('Nut_01','Nut_01',$,(#23654));
#23666=PRESENTATION_STYLE_ASSIGNMENT((#23671));
#23671=SURFACE_STYLE_USAGE(.BOTH.,#23676);
#23676=SURFACE_SIDE_STYLE('',(#23681));
#23681=SURFACE_STYLE_FILL_AREA(#23686);
#23686=FILL_AREA_STYLE('Opaque(210,210,210)',(#23691));
#23691=FILL_AREA_STYLE_COLOUR('Opaque(210,210,210)',#23696);
#23696=COLOUR_RGB('Opaque(210,210,210)', 0.09019608, 0.27058824, 0.51372549);
ENDSEC;
END-ISO-10303-21;
